ISO-10303-21;
HEADER;
/* Generated by software containing ST-Developer
 * from STEP Tools, Inc. (www.steptools.com) 
 */

FILE_DESCRIPTION(
/* description */ ('Bin tilter linkage'),
/* implementation_level */ '2;1');

FILE_NAME(
/* name */ 'M4 short cap screw (27).step',
/* time_stamp */ '2026-10-28T03:26:24-07:00',
/* author */ (''),
/* organization */ (''),
/* preprocessor_version */ 'ST-DEVELOPER v20.2',
/* originating_system */ 'Autodesk Translation Framework v15.17.0.0',
/* authorisation */ '');

FILE_SCHEMA (('AUTOMOTIVE_DESIGN { 1 0 10303 214 3 1 1 }'));
ENDSEC;

DATA;
#10=MECHANICAL_DESIGN_GEOMETRIC_PRESENTATION_REPRESENTATION('',(#928),#23728);
#716=SHAPE_REPRESENTATION_RELATIONSHIP('SRR','None',#24182,#822);
#822=ADVANCED_BREP_SHAPE_REPRESENTATION('',(#1041),#23682);
#928=STYLED_ITEM('',(#24772),#1041);
#1041=MANIFOLD_SOLID_BREP('Body1',#12459);
#1371=FACE_BOUND('',#3424,.T.);
#1720=PLANE('',#14703);
#1721=PLANE('',#14708);
#1722=PLANE('',#14711);
#2362=FACE_OUTER_BOUND('',#3423,.T.);
#2363=FACE_OUTER_BOUND('',#3425,.T.);
#2364=FACE_OUTER_BOUND('',#3426,.T.);
#2365=FACE_OUTER_BOUND('',#3427,.T.);
#2366=FACE_OUTER_BOUND('',#3428,.T.);
#3423=EDGE_LOOP('',(#10117));
#3424=EDGE_LOOP('',(#10118));
#3425=EDGE_LOOP('',(#10119,#10120,#10121,#10122));
#3426=EDGE_LOOP('',(#10123));
#3427=EDGE_LOOP('',(#10124,#10125,#10126,#10127));
#3428=EDGE_LOOP('',(#10128));
#4237=LINE('',#21747,#4912);
#4238=LINE('',#21753,#4913);
#4912=VECTOR('',#17924,0.350000000000001);
#4913=VECTOR('',#17933,0.199999999999999);
#5683=CIRCLE('',#14704,0.350000000000001);
#5684=CIRCLE('',#14705,0.199999999999999);
#5685=CIRCLE('',#14707,0.350000000000001);
#5686=CIRCLE('',#14710,0.199999999999999);
#6537=VERTEX_POINT('',#21741);
#6538=VERTEX_POINT('',#21743);
#6539=VERTEX_POINT('',#21746);
#6540=VERTEX_POINT('',#21751);
#7798=EDGE_CURVE('',#6537,#6537,#5683,.T.);
#7799=EDGE_CURVE('',#6538,#6538,#5684,.T.);
#7800=EDGE_CURVE('',#6537,#6539,#4237,.T.);
#7801=EDGE_CURVE('',#6539,#6539,#5685,.T.);
#7802=EDGE_CURVE('',#6540,#6540,#5686,.T.);
#7803=EDGE_CURVE('',#6540,#6538,#4238,.T.);
#10117=ORIENTED_EDGE('',*,*,#7798,.T.);
#10118=ORIENTED_EDGE('',*,*,#7799,.F.);
#10119=ORIENTED_EDGE('',*,*,#7798,.F.);
#10120=ORIENTED_EDGE('',*,*,#7800,.T.);
#10121=ORIENTED_EDGE('',*,*,#7801,.T.);
#10122=ORIENTED_EDGE('',*,*,#7800,.F.);
#10123=ORIENTED_EDGE('',*,*,#7801,.F.);
#10124=ORIENTED_EDGE('',*,*,#7802,.F.);
#10125=ORIENTED_EDGE('',*,*,#7803,.T.);
#10126=ORIENTED_EDGE('',*,*,#7799,.T.);
#10127=ORIENTED_EDGE('',*,*,#7803,.F.);
#10128=ORIENTED_EDGE('',*,*,#7802,.T.);
#11507=CYLINDRICAL_SURFACE('',#14706,0.350000000000001);
#11508=CYLINDRICAL_SURFACE('',#14709,0.199999999999999);
#12087=ADVANCED_FACE('',(#2362,#1371),#1720,.T.);
#12088=ADVANCED_FACE('',(#2363),#11507,.T.);
#12089=ADVANCED_FACE('',(#2364),#1721,.F.);
#12090=ADVANCED_FACE('',(#2365),#11508,.T.);
#12091=ADVANCED_FACE('',(#2366),#1722,.T.);
#12459=CLOSED_SHELL('',(#12087,#12088,#12089,#12090,#12091));
#14702=AXIS2_PLACEMENT_3D('',#21739,#17914,#17915);
#14703=AXIS2_PLACEMENT_3D('',#21740,#17916,#17917);
#14704=AXIS2_PLACEMENT_3D('',#21742,#17918,#17919);
#14705=AXIS2_PLACEMENT_3D('',#21744,#17920,#17921);
#14706=AXIS2_PLACEMENT_3D('',#21745,#17922,#17923);
#14707=AXIS2_PLACEMENT_3D('',#21748,#17925,#17926);
#14708=AXIS2_PLACEMENT_3D('',#21749,#17927,#17928);
#14709=AXIS2_PLACEMENT_3D('',#21750,#17929,#17930);
#14710=AXIS2_PLACEMENT_3D('',#21752,#17931,#17932);
#14711=AXIS2_PLACEMENT_3D('',#21754,#17934,#17935);
#17914=DIRECTION('axis',(0.,0.,1.));
#17915=DIRECTION('refdir',(1.,0.,0.));
#17916=DIRECTION('center_axis',(0.,1.,0.));
#17917=DIRECTION('ref_axis',(1.,0.,0.));
#17918=DIRECTION('center_axis',(0.,1.,0.));
#17919=DIRECTION('ref_axis',(1.,0.,0.));
#17920=DIRECTION('center_axis',(0.,1.,0.));
#17921=DIRECTION('ref_axis',(1.,0.,0.));
#17922=DIRECTION('center_axis',(0.,1.,0.));
#17923=DIRECTION('ref_axis',(1.,0.,0.));
#17924=DIRECTION('',(0.,-1.,0.));
#17925=DIRECTION('center_axis',(0.,1.,0.));
#17926=DIRECTION('ref_axis',(1.,0.,0.));
#17927=DIRECTION('center_axis',(0.,1.,0.));
#17928=DIRECTION('ref_axis',(1.,0.,0.));
#17929=DIRECTION('center_axis',(0.,1.,0.));
#17930=DIRECTION('ref_axis',(1.,0.,0.));
#17931=DIRECTION('center_axis',(0.,1.,0.));
#17932=DIRECTION('ref_axis',(1.,0.,0.));
#17933=DIRECTION('',(0.,-1.,0.));
#17934=DIRECTION('center_axis',(0.,1.,0.));
#17935=DIRECTION('ref_axis',(1.,0.,0.));
#21739=CARTESIAN_POINT('',(0.,0.,0.));
#21740=CARTESIAN_POINT('Origin',(25.5102260242172,-0.8,27.3496056572921));
#21741=CARTESIAN_POINT('',(25.1602260242172,-0.8,27.3496056572921));
#21742=CARTESIAN_POINT('Origin',(25.5102260242172,-0.8,27.3496056572921));
#21743=CARTESIAN_POINT('',(25.3102260242172,-0.8,27.3496056572921));
#21744=CARTESIAN_POINT('Origin',(25.5102260242172,-0.8,27.3496056572921));
#21745=CARTESIAN_POINT('Origin',(25.5102260242172,-1.2,27.3496056572921));
#21746=CARTESIAN_POINT('',(25.1602260242172,-1.2,27.3496056572921));
#21747=CARTESIAN_POINT('',(25.1602260242172,-1.2,27.3496056572921));
#21748=CARTESIAN_POINT('Origin',(25.5102260242172,-1.2,27.3496056572921));
#21749=CARTESIAN_POINT('Origin',(25.5102260242172,-1.2,27.3496056572921));
#21750=CARTESIAN_POINT('Origin',(25.5102260242172,-0.8,27.3496056572921));
#21751=CARTESIAN_POINT('',(25.3102260242172,-0.1,27.3496056572921));
#21752=CARTESIAN_POINT('Origin',(25.5102260242172,-0.1,27.3496056572921));
#21753=CARTESIAN_POINT('',(25.3102260242172,-0.8,27.3496056572921));
#21754=CARTESIAN_POINT('Origin',(25.5102260242172,-0.1,27.3496056572921));
#23565=UNCERTAINTY_MEASURE_WITH_UNIT(LENGTH_MEASURE(0.001),#23729,
'DISTANCE_ACCURACY_VALUE',
'Maximum model space distance between geometric entities at asserted c
onnectivities');
#23611=UNCERTAINTY_MEASURE_WITH_UNIT(LENGTH_MEASURE(0.001),#23729,
'DISTANCE_ACCURACY_VALUE',
'Maximum model space distance between geometric entities at asserted c
onnectivities');
#23682=(
GEOMETRIC_REPRESENTATION_CONTEXT(3)
GLOBAL_UNCERTAINTY_ASSIGNED_CONTEXT((#23565))
GLOBAL_UNIT_ASSIGNED_CONTEXT((#23729,#23731,#23732))
REPRESENTATION_CONTEXT('','3D')
);
#23728=(
GEOMETRIC_REPRESENTATION_CONTEXT(3)
GLOBAL_UNCERTAINTY_ASSIGNED_CONTEXT((#23611))
GLOBAL_UNIT_ASSIGNED_CONTEXT((#23729,#23731,#23732))
REPRESENTATION_CONTEXT('','3D')
);
#23729=(
LENGTH_UNIT()
NAMED_UNIT(*)
SI_UNIT(.CENTI.,.METRE.)
);
#23731=(
NAMED_UNIT(*)
PLANE_ANGLE_UNIT()
SI_UNIT($,.RADIAN.)
);
#23732=(
NAMED_UNIT(*)
SI_UNIT($,.STERADIAN.)
SOLID_ANGLE_UNIT()
);
#23803=SHAPE_DEFINITION_REPRESENTATION(#23919,#24182);
#23919=PRODUCT_DEFINITION_SHAPE('',$,#24299);
#24182=SHAPE_REPRESENTATION('',(#14702),#23682);
#24228=PRODUCT_DEFINITION_CONTEXT('part definition',#24578,'design');
#24299=PRODUCT_DEFINITION('M4 short cap screw (27)',
'M4 short cap screw (27)',#24415,#24228);
#24415=PRODUCT_DEFINITION_FORMATION('',$,#24650);
#24578=APPLICATION_CONTEXT(
'Core Data for Automotive Mechanical Design Process');
#24579=PRODUCT_CONTEXT('part definition',#24578,'mechanical');
#24650=PRODUCT('M4 short cap screw (27)','M4 short cap screw (27)',
'M4 short cap screw (27)',(#24579));
#24766=COLOUR_RGB('Black',0.12,0.14,0.17);
#24767=FILL_AREA_STYLE_COLOUR('',#24766);
#24768=FILL_AREA_STYLE('',(#24767));
#24769=SURFACE_STYLE_FILL_AREA(#24768);
#24770=SURFACE_SIDE_STYLE('',(#24769));
#24771=SURFACE_STYLE_USAGE(.BOTH.,#24770);
#24772=PRESENTATION_STYLE_ASSIGNMENT((#24771));
ENDSEC;
END-ISO-10303-21;
